ISO-10303-21;
HEADER;
/* Generated by software containing ST-Developer
 * from STEP Tools, Inc. (www.steptools.com) 
 */

FILE_DESCRIPTION(
/* description */ ('PAT-099'),
/* implementation_level */ '2;1');

FILE_NAME(
/* name */ 'M4x10 Cap Screw.step',
/* time_stamp */ '2026-10-29T17:25:42-07:00',
/* author */ (''),
/* organization */ (''),
/* preprocessor_version */ 'ST-DEVELOPER v20.2',
/* originating_system */ 'Autodesk Translation Framework v15.17.0.0',
/* authorisation */ '');

FILE_SCHEMA (('AUTOMOTIVE_DESIGN { 1 0 10303 214 3 1 1 }'));
ENDSEC;

DATA;
#10=MECHANICAL_DESIGN_GEOMETRIC_PRESENTATION_REPRESENTATION('',(#356),#11035);
#33=CONICAL_SURFACE('',#5484,0.325,0.785398163397448);
#34=CONICAL_SURFACE('',#5488,0.335,0.785398163397448);
#35=CONICAL_SURFACE('',#5492,0.21,0.463647609000806);
#41=ORIENTED_CLOSED_SHELL('',*,#4725,.F.);
#43=BREP_WITH_VOIDS('Body1',#4726,(#41));
#306=SHAPE_REPRESENTATION_RELATIONSHIP('SRR','None',#11177,#331);
#331=ADVANCED_BREP_SHAPE_REPRESENTATION('',(#43),#11027);
#356=STYLED_ITEM('',(#11393),#43);
#513=FACE_BOUND('',#1280,.T.);
#631=PLANE('',#5472);
#632=PLANE('',#5473);
#633=PLANE('',#5474);
#634=PLANE('',#5475);
#635=PLANE('',#5476);
#636=PLANE('',#5477);
#637=PLANE('',#5478);
#638=PLANE('',#5479);
#639=PLANE('',#5480);
#640=PLANE('',#5482);
#641=PLANE('',#5490);
#873=FACE_OUTER_BOUND('',#1266,.T.);
#874=FACE_OUTER_BOUND('',#1267,.T.);
#875=FACE_OUTER_BOUND('',#1268,.T.);
#876=FACE_OUTER_BOUND('',#1269,.T.);
#877=FACE_OUTER_BOUND('',#1270,.T.);
#878=FACE_OUTER_BOUND('',#1271,.T.);
#879=FACE_OUTER_BOUND('',#1272,.T.);
#880=FACE_OUTER_BOUND('',#1273,.T.);
#881=FACE_OUTER_BOUND('',#1274,.T.);
#882=FACE_OUTER_BOUND('',#1275,.T.);
#883=FACE_OUTER_BOUND('',#1276,.T.);
#884=FACE_OUTER_BOUND('',#1277,.T.);
#885=FACE_OUTER_BOUND('',#1278,.T.);
#886=FACE_OUTER_BOUND('',#1279,.T.);
#887=FACE_OUTER_BOUND('',#1281,.T.);
#888=FACE_OUTER_BOUND('',#1282,.T.);
#1266=EDGE_LOOP('',(#4037,#4038,#4039,#4040));
#1267=EDGE_LOOP('',(#4041,#4042,#4043,#4044));
#1268=EDGE_LOOP('',(#4045,#4046,#4047,#4048));
#1269=EDGE_LOOP('',(#4049,#4050,#4051,#4052));
#1270=EDGE_LOOP('',(#4053,#4054,#4055,#4056));
#1271=EDGE_LOOP('',(#4057,#4058,#4059,#4060));
#1272=EDGE_LOOP('',(#4061,#4062,#4063,#4064,#4065,#4066));
#1273=EDGE_LOOP('',(#4067,#4068,#4069,#4070,#4071,#4072));
#1274=EDGE_LOOP('',(#4073));
#1275=EDGE_LOOP('',(#4074));
#1276=EDGE_LOOP('',(#4075,#4076,#4077,#4078));
#1277=EDGE_LOOP('',(#4079,#4080,#4081,#4082));
#1278=EDGE_LOOP('',(#4083,#4084,#4085,#4086));
#1279=EDGE_LOOP('',(#4087));
#1280=EDGE_LOOP('',(#4088));
#1281=EDGE_LOOP('',(#4089,#4090,#4091,#4092));
#1282=EDGE_LOOP('',(#4093,#4094,#4095,#4096));
#1556=LINE('',#10283,#1808);
#1557=LINE('',#10285,#1809);
#1558=LINE('',#10287,#1810);
#1559=LINE('',#10288,#1811);
#1560=LINE('',#10291,#1812);
#1561=LINE('',#10293,#1813);
#1562=LINE('',#10294,#1814);
#1563=LINE('',#10297,#1815);
#1564=LINE('',#10299,#1816);
#1565=LINE('',#10300,#1817);
#1566=LINE('',#10303,#1818);
#1567=LINE('',#10305,#1819);
#1568=LINE('',#10306,#1820);
#1569=LINE('',#10309,#1821);
#1570=LINE('',#10311,#1822);
#1571=LINE('',#10312,#1823);
#1572=LINE('',#10314,#1824);
#1573=LINE('',#10315,#1825);
#1574=LINE('',#10327,#1826);
#1575=LINE('',#10331,#1827);
#1576=LINE('',#10335,#1828);
#1577=LINE('',#10342,#1829);
#1578=LINE('',#10344,#1830);
#1808=VECTOR('',#6795,1.);
#1809=VECTOR('',#6796,1.);
#1810=VECTOR('',#6797,1.);
#1811=VECTOR('',#6798,1.);
#1812=VECTOR('',#6801,1.);
#1813=VECTOR('',#6802,1.);
#1814=VECTOR('',#6803,1.);
#1815=VECTOR('',#6806,1.);
#1816=VECTOR('',#6807,1.);
#1817=VECTOR('',#6808,1.);
#1818=VECTOR('',#6811,1.);
#1819=VECTOR('',#6812,1.);
#1820=VECTOR('',#6813,1.);
#1821=VECTOR('',#6816,1.);
#1822=VECTOR('',#6817,1.);
#1823=VECTOR('',#6818,1.);
#1824=VECTOR('',#6821,1.);
#1825=VECTOR('',#6822,1.);
#1826=VECTOR('',#6839,0.325);
#1827=VECTOR('',#6844,0.35);
#1828=VECTOR('',#6849,0.335);
#1829=VECTOR('',#6858,0.21);
#1830=VECTOR('',#6861,0.2);
#2059=CIRCLE('',#5481,0.1954);
#2060=CIRCLE('',#5483,0.3);
#2061=CIRCLE('',#5485,0.35);
#2062=CIRCLE('',#5487,0.35);
#2063=CIRCLE('',#5489,0.32);
#2064=CIRCLE('',#5491,0.22);
#2065=CIRCLE('',#5493,0.1954);
#2443=VERTEX_POINT('',#10281);
#2444=VERTEX_POINT('',#10282);
#2445=VERTEX_POINT('',#10284);
#2446=VERTEX_POINT('',#10286);
#2447=VERTEX_POINT('',#10290);
#2448=VERTEX_POINT('',#10292);
#2449=VERTEX_POINT('',#10296);
#2450=VERTEX_POINT('',#10298);
#2451=VERTEX_POINT('',#10302);
#2452=VERTEX_POINT('',#10304);
#2453=VERTEX_POINT('',#10308);
#2454=VERTEX_POINT('',#10310);
#2455=VERTEX_POINT('',#10319);
#2456=VERTEX_POINT('',#10322);
#2457=VERTEX_POINT('',#10325);
#2458=VERTEX_POINT('',#10329);
#2459=VERTEX_POINT('',#10333);
#2460=VERTEX_POINT('',#10337);
#2461=VERTEX_POINT('',#10340);
#2995=EDGE_CURVE('',#2443,#2444,#1556,.T.);
#2996=EDGE_CURVE('',#2444,#2445,#1557,.T.);
#2997=EDGE_CURVE('',#2445,#2446,#1558,.T.);
#2998=EDGE_CURVE('',#2443,#2446,#1559,.T.);
#2999=EDGE_CURVE('',#2444,#2447,#1560,.T.);
#3000=EDGE_CURVE('',#2447,#2448,#1561,.T.);
#3001=EDGE_CURVE('',#2448,#2445,#1562,.T.);
#3002=EDGE_CURVE('',#2447,#2449,#1563,.T.);
#3003=EDGE_CURVE('',#2449,#2450,#1564,.T.);
#3004=EDGE_CURVE('',#2450,#2448,#1565,.T.);
#3005=EDGE_CURVE('',#2449,#2451,#1566,.T.);
#3006=EDGE_CURVE('',#2451,#2452,#1567,.T.);
#3007=EDGE_CURVE('',#2452,#2450,#1568,.T.);
#3008=EDGE_CURVE('',#2451,#2453,#1569,.T.);
#3009=EDGE_CURVE('',#2453,#2454,#1570,.T.);
#3010=EDGE_CURVE('',#2454,#2452,#1571,.T.);
#3011=EDGE_CURVE('',#2453,#2443,#1572,.T.);
#3012=EDGE_CURVE('',#2446,#2454,#1573,.T.);
#3013=EDGE_CURVE('',#2455,#2455,#2059,.T.);
#3014=EDGE_CURVE('',#2456,#2456,#2060,.T.);
#3015=EDGE_CURVE('',#2457,#2457,#2061,.T.);
#3016=EDGE_CURVE('',#2457,#2456,#1574,.T.);
#3017=EDGE_CURVE('',#2458,#2458,#2062,.T.);
#3018=EDGE_CURVE('',#2458,#2457,#1575,.T.);
#3019=EDGE_CURVE('',#2459,#2459,#2063,.T.);
#3020=EDGE_CURVE('',#2459,#2458,#1576,.T.);
#3021=EDGE_CURVE('',#2460,#2460,#2064,.T.);
#3022=EDGE_CURVE('',#2461,#2461,#2065,.F.);
#3023=EDGE_CURVE('',#2461,#2460,#1577,.T.);
#3024=EDGE_CURVE('',#2455,#2461,#1578,.T.);
#4037=ORIENTED_EDGE('',*,*,#2995,.T.);
#4038=ORIENTED_EDGE('',*,*,#2996,.T.);
#4039=ORIENTED_EDGE('',*,*,#2997,.T.);
#4040=ORIENTED_EDGE('',*,*,#2998,.F.);
#4041=ORIENTED_EDGE('',*,*,#2999,.T.);
#4042=ORIENTED_EDGE('',*,*,#3000,.T.);
#4043=ORIENTED_EDGE('',*,*,#3001,.T.);
#4044=ORIENTED_EDGE('',*,*,#2996,.F.);
#4045=ORIENTED_EDGE('',*,*,#3002,.T.);
#4046=ORIENTED_EDGE('',*,*,#3003,.T.);
#4047=ORIENTED_EDGE('',*,*,#3004,.T.);
#4048=ORIENTED_EDGE('',*,*,#3000,.F.);
#4049=ORIENTED_EDGE('',*,*,#3005,.T.);
#4050=ORIENTED_EDGE('',*,*,#3006,.T.);
#4051=ORIENTED_EDGE('',*,*,#3007,.T.);
#4052=ORIENTED_EDGE('',*,*,#3003,.F.);
#4053=ORIENTED_EDGE('',*,*,#3008,.T.);
#4054=ORIENTED_EDGE('',*,*,#3009,.T.);
#4055=ORIENTED_EDGE('',*,*,#3010,.T.);
#4056=ORIENTED_EDGE('',*,*,#3006,.F.);
#4057=ORIENTED_EDGE('',*,*,#3011,.T.);
#4058=ORIENTED_EDGE('',*,*,#2998,.T.);
#4059=ORIENTED_EDGE('',*,*,#3012,.T.);
#4060=ORIENTED_EDGE('',*,*,#3009,.F.);
#4061=ORIENTED_EDGE('',*,*,#3011,.F.);
#4062=ORIENTED_EDGE('',*,*,#3008,.F.);
#4063=ORIENTED_EDGE('',*,*,#3005,.F.);
#4064=ORIENTED_EDGE('',*,*,#3002,.F.);
#4065=ORIENTED_EDGE('',*,*,#2999,.F.);
#4066=ORIENTED_EDGE('',*,*,#2995,.F.);
#4067=ORIENTED_EDGE('',*,*,#3012,.F.);
#4068=ORIENTED_EDGE('',*,*,#2997,.F.);
#4069=ORIENTED_EDGE('',*,*,#3001,.F.);
#4070=ORIENTED_EDGE('',*,*,#3004,.F.);
#4071=ORIENTED_EDGE('',*,*,#3007,.F.);
#4072=ORIENTED_EDGE('',*,*,#3010,.F.);
#4073=ORIENTED_EDGE('',*,*,#3013,.F.);
#4074=ORIENTED_EDGE('',*,*,#3014,.F.);
#4075=ORIENTED_EDGE('',*,*,#3015,.F.);
#4076=ORIENTED_EDGE('',*,*,#3016,.T.);
#4077=ORIENTED_EDGE('',*,*,#3014,.T.);
#4078=ORIENTED_EDGE('',*,*,#3016,.F.);
#4079=ORIENTED_EDGE('',*,*,#3017,.F.);
#4080=ORIENTED_EDGE('',*,*,#3018,.T.);
#4081=ORIENTED_EDGE('',*,*,#3015,.T.);
#4082=ORIENTED_EDGE('',*,*,#3018,.F.);
#4083=ORIENTED_EDGE('',*,*,#3019,.F.);
#4084=ORIENTED_EDGE('',*,*,#3020,.T.);
#4085=ORIENTED_EDGE('',*,*,#3017,.T.);
#4086=ORIENTED_EDGE('',*,*,#3020,.F.);
#4087=ORIENTED_EDGE('',*,*,#3019,.T.);
#4088=ORIENTED_EDGE('',*,*,#3021,.F.);
#4089=ORIENTED_EDGE('',*,*,#3022,.F.);
#4090=ORIENTED_EDGE('',*,*,#3023,.T.);
#4091=ORIENTED_EDGE('',*,*,#3021,.T.);
#4092=ORIENTED_EDGE('',*,*,#3023,.F.);
#4093=ORIENTED_EDGE('',*,*,#3013,.T.);
#4094=ORIENTED_EDGE('',*,*,#3024,.T.);
#4095=ORIENTED_EDGE('',*,*,#3022,.T.);
#4096=ORIENTED_EDGE('',*,*,#3024,.F.);
#4410=CYLINDRICAL_SURFACE('',#5486,0.35);
#4411=CYLINDRICAL_SURFACE('',#5494,0.1954);
#4638=ADVANCED_FACE('',(#873),#631,.F.);
#4639=ADVANCED_FACE('',(#874),#632,.F.);
#4640=ADVANCED_FACE('',(#875),#633,.F.);
#4641=ADVANCED_FACE('',(#876),#634,.F.);
#4642=ADVANCED_FACE('',(#877),#635,.F.);
#4643=ADVANCED_FACE('',(#878),#636,.F.);
#4644=ADVANCED_FACE('',(#879),#637,.F.);
#4645=ADVANCED_FACE('',(#880),#638,.F.);
#4646=ADVANCED_FACE('',(#881),#639,.F.);
#4647=ADVANCED_FACE('',(#882),#640,.T.);
#4648=ADVANCED_FACE('',(#883),#33,.T.);
#4649=ADVANCED_FACE('',(#884),#4410,.T.);
#4650=ADVANCED_FACE('',(#885),#34,.T.);
#4651=ADVANCED_FACE('',(#886,#513),#641,.T.);
#4652=ADVANCED_FACE('',(#887),#35,.T.);
#4653=ADVANCED_FACE('',(#888),#4411,.T.);
#4725=CLOSED_SHELL('',(#4638,#4639,#4640,#4641,#4642,#4643,#4644,#4645));
#4726=CLOSED_SHELL('',(#4646,#4647,#4648,#4649,#4650,#4651,#4652,#4653));
#5471=AXIS2_PLACEMENT_3D('',#10279,#6791,#6792);
#5472=AXIS2_PLACEMENT_3D('',#10280,#6793,#6794);
#5473=AXIS2_PLACEMENT_3D('',#10289,#6799,#6800);
#5474=AXIS2_PLACEMENT_3D('',#10295,#6804,#6805);
#5475=AXIS2_PLACEMENT_3D('',#10301,#6809,#6810);
#5476=AXIS2_PLACEMENT_3D('',#10307,#6814,#6815);
#5477=AXIS2_PLACEMENT_3D('',#10313,#6819,#6820);
#5478=AXIS2_PLACEMENT_3D('',#10316,#6823,#6824);
#5479=AXIS2_PLACEMENT_3D('',#10317,#6825,#6826);
#5480=AXIS2_PLACEMENT_3D('',#10318,#6827,#6828);
#5481=AXIS2_PLACEMENT_3D('',#10320,#6829,#6830);
#5482=AXIS2_PLACEMENT_3D('',#10321,#6831,#6832);
#5483=AXIS2_PLACEMENT_3D('',#10323,#6833,#6834);
#5484=AXIS2_PLACEMENT_3D('',#10324,#6835,#6836);
#5485=AXIS2_PLACEMENT_3D('',#10326,#6837,#6838);
#5486=AXIS2_PLACEMENT_3D('',#10328,#6840,#6841);
#5487=AXIS2_PLACEMENT_3D('',#10330,#6842,#6843);
#5488=AXIS2_PLACEMENT_3D('',#10332,#6845,#6846);
#5489=AXIS2_PLACEMENT_3D('',#10334,#6847,#6848);
#5490=AXIS2_PLACEMENT_3D('',#10336,#6850,#6851);
#5491=AXIS2_PLACEMENT_3D('',#10338,#6852,#6853);
#5492=AXIS2_PLACEMENT_3D('',#10339,#6854,#6855);
#5493=AXIS2_PLACEMENT_3D('',#10341,#6856,#6857);
#5494=AXIS2_PLACEMENT_3D('',#10343,#6859,#6860);
#6791=DIRECTION('axis',(0.,0.,1.));
#6792=DIRECTION('refdir',(1.,0.,0.));
#6793=DIRECTION('center_axis',(0.866025403784439,0.,-0.5));
#6794=DIRECTION('ref_axis',(0.5,0.,0.866025403784439));
#6795=DIRECTION('',(-0.5,0.,-0.866025403784439));
#6796=DIRECTION('',(0.,-1.,0.));
#6797=DIRECTION('',(0.5,0.,0.866025403784439));
#6798=DIRECTION('',(0.,-1.,0.));
#6799=DIRECTION('center_axis',(1.60246890531964E-16,0.,-1.));
#6800=DIRECTION('ref_axis',(1.,0.,1.60246890531964E-16));
#6801=DIRECTION('',(-1.,0.,-1.60246890531964E-16));
#6802=DIRECTION('',(0.,-1.,0.));
#6803=DIRECTION('',(1.,0.,1.60246890531964E-16));
#6804=DIRECTION('center_axis',(-0.866025403784439,0.,-0.5));
#6805=DIRECTION('ref_axis',(0.5,0.,-0.866025403784439));
#6806=DIRECTION('',(-0.5,0.,0.866025403784439));
#6807=DIRECTION('',(0.,-1.,0.));
#6808=DIRECTION('',(0.5,0.,-0.866025403784439));
#6809=DIRECTION('center_axis',(-0.866025403784439,0.,0.5));
#6810=DIRECTION('ref_axis',(-0.5,0.,-0.866025403784439));
#6811=DIRECTION('',(0.5,0.,0.866025403784439));
#6812=DIRECTION('',(0.,-1.,0.));
#6813=DIRECTION('',(-0.5,0.,-0.866025403784439));
#6814=DIRECTION('center_axis',(-1.60246890531964E-16,0.,1.));
#6815=DIRECTION('ref_axis',(-1.,0.,-1.60246890531964E-16));
#6816=DIRECTION('',(1.,0.,1.60246890531964E-16));
#6817=DIRECTION('',(0.,-1.,0.));
#6818=DIRECTION('',(-1.,0.,-1.60246890531964E-16));
#6819=DIRECTION('center_axis',(0.866025403784439,0.,0.5));
#6820=DIRECTION('ref_axis',(-0.5,0.,0.866025403784439));
#6821=DIRECTION('',(0.5,0.,-0.866025403784439));
#6822=DIRECTION('',(-0.5,0.,0.866025403784439));
#6823=DIRECTION('center_axis',(0.,1.,0.));
#6824=DIRECTION('ref_axis',(1.,0.,0.));
#6825=DIRECTION('center_axis',(0.,-1.,0.));
#6826=DIRECTION('ref_axis',(0.,0.,-1.));
#6827=DIRECTION('center_axis',(0.,1.,0.));
#6828=DIRECTION('ref_axis',(1.,0.,0.));
#6829=DIRECTION('center_axis',(0.,1.,0.));
#6830=DIRECTION('ref_axis',(1.,0.,0.));
#6831=DIRECTION('center_axis',(0.,1.,0.));
#6832=DIRECTION('ref_axis',(0.,0.,1.));
#6833=DIRECTION('center_axis',(0.,-1.,0.));
#6834=DIRECTION('ref_axis',(1.,0.,0.));
#6835=DIRECTION('center_axis',(0.,-1.,0.));
#6836=DIRECTION('ref_axis',(1.,0.,0.));
#6837=DIRECTION('center_axis',(0.,-1.,0.));
#6838=DIRECTION('ref_axis',(1.,0.,0.));
#6839=DIRECTION('',(0.707106781186547,0.707106781186548,8.65956056235493E-17));
#6840=DIRECTION('center_axis',(0.,-1.,0.));
#6841=DIRECTION('ref_axis',(1.,0.,0.));
#6842=DIRECTION('center_axis',(0.,-1.,0.));
#6843=DIRECTION('ref_axis',(1.,0.,0.));
#6844=DIRECTION('',(0.,1.,0.));
#6845=DIRECTION('center_axis',(0.,1.,0.));
#6846=DIRECTION('ref_axis',(1.,0.,0.));
#6847=DIRECTION('center_axis',(0.,-1.,0.));
#6848=DIRECTION('ref_axis',(1.,0.,0.));
#6849=DIRECTION('',(-0.707106781186547,0.707106781186548,-8.65956056235493E-17));
#6850=DIRECTION('center_axis',(0.,-1.,0.));
#6851=DIRECTION('ref_axis',(0.,0.,-1.));
#6852=DIRECTION('center_axis',(0.,-1.,0.));
#6853=DIRECTION('ref_axis',(1.,0.,0.));
#6854=DIRECTION('center_axis',(0.,1.,0.));
#6855=DIRECTION('ref_axis',(1.,0.,0.));
#6856=DIRECTION('center_axis',(0.,1.,0.));
#6857=DIRECTION('ref_axis',(1.,0.,0.));
#6858=DIRECTION('',(-0.447213595499958,0.894427190999916,-5.47678698264203E-17));
#6859=DIRECTION('center_axis',(0.,-1.,0.));
#6860=DIRECTION('ref_axis',(1.,0.,0.));
#6861=DIRECTION('',(0.,1.,0.));
#10279=CARTESIAN_POINT('',(0.,0.,0.));
#10280=CARTESIAN_POINT('Origin',(0.0866025403784439,-0.4,-0.15));
#10281=CARTESIAN_POINT('',(0.173205080756888,-0.4,0.));
#10282=CARTESIAN_POINT('',(0.0866025403784439,-0.4,-0.15));
#10283=CARTESIAN_POINT('',(0.173205080756888,-0.4,0.));
#10284=CARTESIAN_POINT('',(0.0866025403784439,-0.64,-0.15));
#10285=CARTESIAN_POINT('',(0.0866025403784439,-0.4,-0.15));
#10286=CARTESIAN_POINT('',(0.173205080756888,-0.64,0.));
#10287=CARTESIAN_POINT('',(0.173205080756888,-0.64,0.));
#10288=CARTESIAN_POINT('',(0.173205080756888,-0.4,0.));
#10289=CARTESIAN_POINT('Origin',(-0.0866025403784438,-0.4,-0.15));
#10290=CARTESIAN_POINT('',(-0.0866025403784438,-0.4,-0.15));
#10291=CARTESIAN_POINT('',(0.0866025403784439,-0.4,-0.15));
#10292=CARTESIAN_POINT('',(-0.0866025403784438,-0.64,-0.15));
#10293=CARTESIAN_POINT('',(-0.0866025403784438,-0.4,-0.15));
#10294=CARTESIAN_POINT('',(0.0866025403784439,-0.64,-0.15));
#10295=CARTESIAN_POINT('Origin',(-0.173205080756888,-0.4,-2.77555756156289E-17));
#10296=CARTESIAN_POINT('',(-0.173205080756888,-0.4,-2.12115047744981E-17));
#10297=CARTESIAN_POINT('',(-0.0866025403784438,-0.4,-0.15));
#10298=CARTESIAN_POINT('',(-0.173205080756888,-0.64,-2.77555756156289E-17));
#10299=CARTESIAN_POINT('',(-0.173205080756888,-0.4,-2.12115047744981E-17));
#10300=CARTESIAN_POINT('',(-0.0866025403784438,-0.64,-0.15));
#10301=CARTESIAN_POINT('Origin',(-0.0866025403784439,-0.4,0.15));
#10302=CARTESIAN_POINT('',(-0.0866025403784439,-0.4,0.15));
#10303=CARTESIAN_POINT('',(-0.173205080756888,-0.4,-2.12115047744981E-17));
#10304=CARTESIAN_POINT('',(-0.0866025403784439,-0.64,0.15));
#10305=CARTESIAN_POINT('',(-0.0866025403784439,-0.4,0.15));
#10306=CARTESIAN_POINT('',(-0.173205080756888,-0.64,-2.12115047744981E-17));
#10307=CARTESIAN_POINT('Origin',(0.0866025403784439,-0.4,0.15));
#10308=CARTESIAN_POINT('',(0.0866025403784439,-0.4,0.15));
#10309=CARTESIAN_POINT('',(-0.0866025403784439,-0.4,0.15));
#10310=CARTESIAN_POINT('',(0.0866025403784439,-0.64,0.15));
#10311=CARTESIAN_POINT('',(0.0866025403784439,-0.4,0.15));
#10312=CARTESIAN_POINT('',(-0.0866025403784439,-0.64,0.15));
#10313=CARTESIAN_POINT('Origin',(0.173205080756888,-0.4,0.));
#10314=CARTESIAN_POINT('',(0.0866025403784439,-0.4,0.15));
#10315=CARTESIAN_POINT('',(0.0866025403784439,-0.64,0.15));
#10316=CARTESIAN_POINT('Origin',(0.,-0.4,-2.77555756156289E-17));
#10317=CARTESIAN_POINT('Origin',(0.,-0.64,-2.77555756156289E-17));
#10318=CARTESIAN_POINT('Origin',(0.,-1.,0.));
#10319=CARTESIAN_POINT('',(-0.1954,-1.,2.39295984553393E-17));
#10320=CARTESIAN_POINT('Origin',(0.,-1.,0.));
#10321=CARTESIAN_POINT('Origin',(0.3,0.4,0.));
#10322=CARTESIAN_POINT('',(-0.3,0.4,-3.67394039744206E-17));
#10323=CARTESIAN_POINT('Origin',(0.,0.4,0.));
#10324=CARTESIAN_POINT('Origin',(0.,0.375,0.));
#10325=CARTESIAN_POINT('',(-0.35,0.35,-4.28626379701573E-17));
#10326=CARTESIAN_POINT('Origin',(0.,0.35,0.));
#10327=CARTESIAN_POINT('',(-0.325,0.375,-3.9801020972289E-17));
#10328=CARTESIAN_POINT('Origin',(0.,0.19,0.));
#10329=CARTESIAN_POINT('',(-0.35,0.03,-4.28626379701574E-17));
#10330=CARTESIAN_POINT('Origin',(0.,0.03,0.));
#10331=CARTESIAN_POINT('',(-0.35,0.19,-4.28626379701574E-17));
#10332=CARTESIAN_POINT('Origin',(0.,0.0149999999999999,0.));
#10333=CARTESIAN_POINT('',(-0.32,-3.29597460435593E-17,-3.91886975727153E-17));
#10334=CARTESIAN_POINT('Origin',(0.,0.,0.));
#10335=CARTESIAN_POINT('',(-0.335,0.0149999999999999,-4.10256677714363E-17));
#10336=CARTESIAN_POINT('Origin',(0.22,0.,0.));
#10337=CARTESIAN_POINT('',(-0.22,-6.93889390390723E-18,-2.69422295812418E-17));
#10338=CARTESIAN_POINT('Origin',(0.,0.,0.));
#10339=CARTESIAN_POINT('Origin',(0.,-0.02,0.));
#10340=CARTESIAN_POINT('',(-0.1954,-0.0492,2.39295984553393E-17));
#10341=CARTESIAN_POINT('Origin',(0.,-0.0492,0.));
#10342=CARTESIAN_POINT('',(-0.21,-0.02,-2.57175827820944E-17));
#10343=CARTESIAN_POINT('Origin',(0.,-0.8,0.));
#10344=CARTESIAN_POINT('',(-0.1954,-0.8,-2.39295984553393E-17));
#10994=UNCERTAINTY_MEASURE_WITH_UNIT(LENGTH_MEASURE(0.001),#11036,
'DISTANCE_ACCURACY_VALUE',
'Maximum model space distance between geometric entities at asserted c
onnectivities');
#11002=UNCERTAINTY_MEASURE_WITH_UNIT(LENGTH_MEASURE(0.001),#11036,
'DISTANCE_ACCURACY_VALUE',
'Maximum model space distance between geometric entities at asserted c
onnectivities');
#11027=(
GEOMETRIC_REPRESENTATION_CONTEXT(3)
GLOBAL_UNCERTAINTY_ASSIGNED_CONTEXT((#10994))
GLOBAL_UNIT_ASSIGNED_CONTEXT((#11036,#11038,#11039))
REPRESENTATION_CONTEXT('','3D')
);
#11035=(
GEOMETRIC_REPRESENTATION_CONTEXT(3)
GLOBAL_UNCERTAINTY_ASSIGNED_CONTEXT((#11002))
GLOBAL_UNIT_ASSIGNED_CONTEXT((#11036,#11038,#11039))
REPRESENTATION_CONTEXT('','3D')
);
#11036=(
LENGTH_UNIT()
NAMED_UNIT(*)
SI_UNIT(.CENTI.,.METRE.)
);
#11038=(
NAMED_UNIT(*)
PLANE_ANGLE_UNIT()
SI_UNIT($,.RADIAN.)
);
#11039=(
NAMED_UNIT(*)
SI_UNIT($,.STERADIAN.)
SOLID_ANGLE_UNIT()
);
#11064=SHAPE_DEFINITION_REPRESENTATION(#11102,#11177);
#11102=PRODUCT_DEFINITION_SHAPE('',$,#11210);
#11177=SHAPE_REPRESENTATION('',(#5471),#11027);
#11185=PRODUCT_DEFINITION_CONTEXT('part definition',#11283,'design');
#11210=PRODUCT_DEFINITION('M4x10 Cap Screw','M4x10 Cap Screw',#11242,#11185);
#11242=PRODUCT_DEFINITION_FORMATION('',$,#11309);
#11283=APPLICATION_CONTEXT(
'Core Data for Automotive Mechanical Design Process');
#11284=PRODUCT_CONTEXT('part definition',#11283,'mechanical');
#11309=PRODUCT('M4x10 Cap Screw','M4x10 Cap Screw','M4x10 Cap Screw',(#11284));
#11387=COLOUR_RGB('Black',0.12,0.14,0.17);
#11388=FILL_AREA_STYLE_COLOUR('',#11387);
#11389=FILL_AREA_STYLE('',(#11388));
#11390=SURFACE_STYLE_FILL_AREA(#11389);
#11391=SURFACE_SIDE_STYLE('',(#11390));
#11392=SURFACE_STYLE_USAGE(.BOTH.,#11391);
#11393=PRESENTATION_STYLE_ASSIGNMENT((#11392));
ENDSEC;
END-ISO-10303-21;
